ISO-10303-21;
HEADER;
/* Generated by software containing ST-Developer
 * from STEP Tools, Inc. (www.steptools.com) 
 */

FILE_DESCRIPTION(
/* description */ ('Manual piston pump'),
/* implementation_level */ '2;1');

FILE_NAME(
/* name */ 'Flat Washer - M5.step',
/* time_stamp */ '2026-11-02T16:54:23-08:00',
/* author */ (''),
/* organization */ (''),
/* preprocessor_version */ 'ST-DEVELOPER v20.2',
/* originating_system */ 'Autodesk Translation Framework v15.17.0.0',
/* authorisation */ '');

FILE_SCHEMA (('AUTOMOTIVE_DESIGN { 1 0 10303 214 3 1 1 }'));
ENDSEC;

DATA;
#10=MECHANICAL_DESIGN_GEOMETRIC_PRESENTATION_REPRESENTATION('',(#702),#19043);
#531=CONICAL_SURFACE('',#10504,0.275,0.785398163397449);
#576=SHAPE_REPRESENTATION_RELATIONSHIP('SRR','None',#19322,#639);
#639=ADVANCED_BREP_SHAPE_REPRESENTATION('',(#773),#18989);
#702=STYLED_ITEM('',(#19664),#773);
#773=MANIFOLD_SOLID_BREP('Body1',#9487);
#885=FACE_BOUND('',#2058,.T.);
#886=FACE_BOUND('',#2061,.T.);
#1144=CYLINDRICAL_SURFACE('',#10507,0.265);
#1145=CYLINDRICAL_SURFACE('',#10511,0.5);
#1422=FACE_OUTER_BOUND('',#2055,.T.);
#1423=FACE_OUTER_BOUND('',#2056,.T.);
#1424=FACE_OUTER_BOUND('',#2057,.T.);
#1425=FACE_OUTER_BOUND('',#2059,.T.);
#1426=FACE_OUTER_BOUND('',#2060,.T.);
#2055=EDGE_LOOP('',(#6799,#6800,#6801,#6802));
#2056=EDGE_LOOP('',(#6803,#6804,#6805,#6806));
#2057=EDGE_LOOP('',(#6807));
#2058=EDGE_LOOP('',(#6808));
#2059=EDGE_LOOP('',(#6809,#6810,#6811,#6812));
#2060=EDGE_LOOP('',(#6813));
#2061=EDGE_LOOP('',(#6814));
#2777=CIRCLE('',#10505,0.285);
#2778=CIRCLE('',#10506,0.265);
#2779=CIRCLE('',#10508,0.265);
#2780=CIRCLE('',#10510,0.5);
#2781=CIRCLE('',#10512,0.5);
#3293=LINE('',#15241,#3897);
#3294=LINE('',#15245,#3898);
#3295=LINE('',#15252,#3899);
#3897=VECTOR('',#12167,0.275);
#3898=VECTOR('',#12172,0.265);
#3899=VECTOR('',#12181,0.5);
#4528=VERTEX_POINT('',#15238);
#4529=VERTEX_POINT('',#15240);
#4530=VERTEX_POINT('',#15244);
#4531=VERTEX_POINT('',#15248);
#4532=VERTEX_POINT('',#15251);
#5386=EDGE_CURVE('',#4528,#4528,#2777,.T.);
#5387=EDGE_CURVE('',#4528,#4529,#3293,.T.);
#5388=EDGE_CURVE('',#4529,#4529,#2778,.T.);
#5389=EDGE_CURVE('',#4529,#4530,#3294,.T.);
#5390=EDGE_CURVE('',#4530,#4530,#2779,.T.);
#5391=EDGE_CURVE('',#4531,#4531,#2780,.T.);
#5392=EDGE_CURVE('',#4531,#4532,#3295,.T.);
#5393=EDGE_CURVE('',#4532,#4532,#2781,.T.);
#6799=ORIENTED_EDGE('',*,*,#5386,.T.);
#6800=ORIENTED_EDGE('',*,*,#5387,.T.);
#6801=ORIENTED_EDGE('',*,*,#5388,.T.);
#6802=ORIENTED_EDGE('',*,*,#5387,.F.);
#6803=ORIENTED_EDGE('',*,*,#5388,.F.);
#6804=ORIENTED_EDGE('',*,*,#5389,.T.);
#6805=ORIENTED_EDGE('',*,*,#5390,.T.);
#6806=ORIENTED_EDGE('',*,*,#5389,.F.);
#6807=ORIENTED_EDGE('',*,*,#5391,.T.);
#6808=ORIENTED_EDGE('',*,*,#5386,.F.);
#6809=ORIENTED_EDGE('',*,*,#5391,.F.);
#6810=ORIENTED_EDGE('',*,*,#5392,.T.);
#6811=ORIENTED_EDGE('',*,*,#5393,.T.);
#6812=ORIENTED_EDGE('',*,*,#5392,.F.);
#6813=ORIENTED_EDGE('',*,*,#5393,.F.);
#6814=ORIENTED_EDGE('',*,*,#5390,.F.);
#8645=PLANE('',#10509);
#8646=PLANE('',#10513);
#9027=ADVANCED_FACE('',(#1422),#531,.F.);
#9028=ADVANCED_FACE('',(#1423),#1144,.F.);
#9029=ADVANCED_FACE('',(#1424,#885),#8645,.T.);
#9030=ADVANCED_FACE('',(#1425),#1145,.T.);
#9031=ADVANCED_FACE('',(#1426,#886),#8646,.F.);
#9487=CLOSED_SHELL('',(#9027,#9028,#9029,#9030,#9031));
#10503=AXIS2_PLACEMENT_3D('',#15236,#12161,#12162);
#10504=AXIS2_PLACEMENT_3D('',#15237,#12163,#12164);
#10505=AXIS2_PLACEMENT_3D('',#15239,#12165,#12166);
#10506=AXIS2_PLACEMENT_3D('',#15242,#12168,#12169);
#10507=AXIS2_PLACEMENT_3D('',#15243,#12170,#12171);
#10508=AXIS2_PLACEMENT_3D('',#15246,#12173,#12174);
#10509=AXIS2_PLACEMENT_3D('',#15247,#12175,#12176);
#10510=AXIS2_PLACEMENT_3D('',#15249,#12177,#12178);
#10511=AXIS2_PLACEMENT_3D('',#15250,#12179,#12180);
#10512=AXIS2_PLACEMENT_3D('',#15253,#12182,#12183);
#10513=AXIS2_PLACEMENT_3D('',#15254,#12184,#12185);
#12161=DIRECTION('axis',(0.,0.,1.));
#12162=DIRECTION('refdir',(1.,0.,0.));
#12163=DIRECTION('center_axis',(0.,1.,0.));
#12164=DIRECTION('ref_axis',(1.,0.,0.));
#12165=DIRECTION('center_axis',(0.,1.,0.));
#12166=DIRECTION('ref_axis',(1.,0.,0.));
#12167=DIRECTION('',(0.707106781186548,-0.707106781186547,-8.65956056235494E-17));
#12168=DIRECTION('center_axis',(0.,-1.,0.));
#12169=DIRECTION('ref_axis',(1.,0.,0.));
#12170=DIRECTION('center_axis',(0.,1.,0.));
#12171=DIRECTION('ref_axis',(1.,0.,0.));
#12172=DIRECTION('',(0.,-1.,0.));
#12173=DIRECTION('center_axis',(0.,-1.,0.));
#12174=DIRECTION('ref_axis',(1.,0.,0.));
#12175=DIRECTION('center_axis',(0.,1.,0.));
#12176=DIRECTION('ref_axis',(1.,0.,0.));
#12177=DIRECTION('center_axis',(0.,1.,0.));
#12178=DIRECTION('ref_axis',(1.,0.,0.));
#12179=DIRECTION('center_axis',(0.,1.,0.));
#12180=DIRECTION('ref_axis',(1.,0.,0.));
#12181=DIRECTION('',(0.,-1.,0.));
#12182=DIRECTION('center_axis',(0.,1.,0.));
#12183=DIRECTION('ref_axis',(1.,0.,0.));
#12184=DIRECTION('center_axis',(0.,1.,0.));
#12185=DIRECTION('ref_axis',(1.,0.,0.));
#15236=CARTESIAN_POINT('',(0.,0.,0.));
#15237=CARTESIAN_POINT('Origin',(0.,0.09,0.));
#15238=CARTESIAN_POINT('',(-0.285,0.1,3.49024337756996E-17));
#15239=CARTESIAN_POINT('Origin',(0.,0.1,0.));
#15240=CARTESIAN_POINT('',(-0.265,0.08,-3.24531401774049E-17));
#15241=CARTESIAN_POINT('',(-0.275,0.09,3.36777869765522E-17));
#15242=CARTESIAN_POINT('Origin',(0.,0.08,0.));
#15243=CARTESIAN_POINT('Origin',(0.,0.,0.));
#15244=CARTESIAN_POINT('',(-0.265,0.,3.24531401774049E-17));
#15245=CARTESIAN_POINT('',(-0.265,0.,3.24531401774049E-17));
#15246=CARTESIAN_POINT('Origin',(0.,0.,0.));
#15247=CARTESIAN_POINT('Origin',(0.,0.1,0.));
#15248=CARTESIAN_POINT('',(-0.5,0.1,6.12323399573677E-17));
#15249=CARTESIAN_POINT('Origin',(0.,0.1,0.));
#15250=CARTESIAN_POINT('Origin',(0.,0.,0.));
#15251=CARTESIAN_POINT('',(-0.5,0.,6.12323399573677E-17));
#15252=CARTESIAN_POINT('',(-0.5,0.,6.12323399573677E-17));
#15253=CARTESIAN_POINT('Origin',(0.,0.,0.));
#15254=CARTESIAN_POINT('Origin',(0.,0.,0.));
#18918=UNCERTAINTY_MEASURE_WITH_UNIT(LENGTH_MEASURE(0.001),#19044,
'DISTANCE_ACCURACY_VALUE',
'Maximum model space distance between geometric entities at asserted c
onnectivities');
#18972=UNCERTAINTY_MEASURE_WITH_UNIT(LENGTH_MEASURE(0.001),#19044,
'DISTANCE_ACCURACY_VALUE',
'Maximum model space distance between geometric entities at asserted c
onnectivities');
#18989=(
GEOMETRIC_REPRESENTATION_CONTEXT(3)
GLOBAL_UNCERTAINTY_ASSIGNED_CONTEXT((#18918))
GLOBAL_UNIT_ASSIGNED_CONTEXT((#19044,#19046,#19047))
REPRESENTATION_CONTEXT('','3D')
);
#19043=(
GEOMETRIC_REPRESENTATION_CONTEXT(3)
GLOBAL_UNCERTAINTY_ASSIGNED_CONTEXT((#18972))
GLOBAL_UNIT_ASSIGNED_CONTEXT((#19044,#19046,#19047))
REPRESENTATION_CONTEXT('','3D')
);
#19044=(
LENGTH_UNIT()
NAMED_UNIT(*)
SI_UNIT(.CENTI.,.METRE.)
);
#19046=(
NAMED_UNIT(*)
PLANE_ANGLE_UNIT()
SI_UNIT($,.RADIAN.)
);
#19047=(
NAMED_UNIT(*)
SI_UNIT($,.STERADIAN.)
SOLID_ANGLE_UNIT()
);
#19064=SHAPE_DEFINITION_REPRESENTATION(#19134,#19322);
#19134=PRODUCT_DEFINITION_SHAPE('',$,#19393);
#19322=SHAPE_REPRESENTATION('',(#10503),#18989);
#19376=PRODUCT_DEFINITION_CONTEXT('part definition',#19588,'design');
#19393=PRODUCT_DEFINITION('2026-11-03-00-38-46-455','Flat Washer - M5',
#19463,#19376);
#19463=PRODUCT_DEFINITION_FORMATION('',$,#19606);
#19588=APPLICATION_CONTEXT(
'Core Data for Automotive Mechanical Design Process');
#19589=PRODUCT_CONTEXT('part definition',#19588,'mechanical');
#19606=PRODUCT('2026-11-03-00-38-46-455','Flat Washer - M5',
'Flat Washer - M5',(#19589));
#19664=PRESENTATION_STYLE_ASSIGNMENT((#19670));
#19670=SURFACE_STYLE_USAGE(.BOTH.,#19676);
#19676=SURFACE_SIDE_STYLE('',(#19682));
#19682=SURFACE_STYLE_FILL_AREA(#19688);
#19688=FILL_AREA_STYLE('CAD Library Painted - Steel gray',(#19694));
#19694=FILL_AREA_STYLE_COLOUR('CAD Library Painted - Steel gray',#19700);
#19700=COLOUR_RGB('CAD Library Painted - Steel gray',0.592156862745098,
0.631372549019608,0.67843137254902);
ENDSEC;
END-ISO-10303-21;
